ISO-10303-21;
HEADER;
/* Generated by software containing ST-Developer
 * from STEP Tools, Inc. (www.steptools.com) 
 */

FILE_DESCRIPTION(
/* description */ (''),
/* implementation_level */ '2;1');

FILE_NAME(
/* name */ 'Screw_02.step',
/* time_stamp */ '2026-10-04T23:23:09-07:00',
/* author */ (''),
/* organization */ (''),
/* preprocessor_version */ 'ST-DEVELOPER v20.2',
/* originating_system */ 'Autodesk Translation Framework v15.15.0.0',
/* authorisation */ '');

FILE_SCHEMA (('AUTOMOTIVE_DESIGN { 1 0 10303 214 3 1 1 }'));
ENDSEC;

DATA;
#10=MECHANICAL_DESIGN_GEOMETRIC_PRESENTATION_REPRESENTATION('',(#66,#67),#2676);
#43=SPHERICAL_SURFACE('',#1637,1.);
#50=SHAPE_REPRESENTATION_RELATIONSHIP('SRR','None',#2709,#58);
#58=ADVANCED_BREP_SHAPE_REPRESENTATION('',(#77,#78),#2669);
#66=STYLED_ITEM('',(#2757),#77);
#67=STYLED_ITEM('',(#2757),#78);
#77=MANIFOLD_SOLID_BREP('Body1',#1477);
#78=MANIFOLD_SOLID_BREP('Body1',#1478);
#91=CYLINDRICAL_SURFACE('',#1610,1.);
#92=CYLINDRICAL_SURFACE('',#1614,2.);
#93=CYLINDRICAL_SURFACE('',#1622,1.);
#94=CYLINDRICAL_SURFACE('',#1626,1.);
#95=CYLINDRICAL_SURFACE('',#1630,2.);
#114=FACE_BOUND('',#308,.T.);
#115=FACE_BOUND('',#313,.T.);
#116=FACE_BOUND('',#316,.T.);
#117=FACE_BOUND('',#321,.T.);
#118=FACE_BOUND('',#325,.T.);
#145=PLANE('',#1607);
#146=PLANE('',#1616);
#147=PLANE('',#1619);
#148=PLANE('',#1624);
#149=PLANE('',#1628);
#150=PLANE('',#1634);
#204=FACE_OUTER_BOUND('',#307,.T.);
#205=FACE_OUTER_BOUND('',#309,.T.);
#206=FACE_OUTER_BOUND('',#310,.T.);
#207=FACE_OUTER_BOUND('',#311,.T.);
#208=FACE_OUTER_BOUND('',#312,.T.);
#209=FACE_OUTER_BOUND('',#314,.T.);
#210=FACE_OUTER_BOUND('',#315,.T.);
#211=FACE_OUTER_BOUND('',#317,.T.);
#212=FACE_OUTER_BOUND('',#318,.T.);
#213=FACE_OUTER_BOUND('',#319,.T.);
#214=FACE_OUTER_BOUND('',#320,.T.);
#215=FACE_OUTER_BOUND('',#322,.T.);
#216=FACE_OUTER_BOUND('',#323,.T.);
#217=FACE_OUTER_BOUND('',#324,.T.);
#218=FACE_OUTER_BOUND('',#326,.T.);
#219=FACE_OUTER_BOUND('',#327,.T.);
#307=EDGE_LOOP('',(#1064));
#308=EDGE_LOOP('',(#1065));
#309=EDGE_LOOP('',(#1066,#1067,#1068,#1069));
#310=EDGE_LOOP('',(#1070,#1071,#1072,#1073));
#311=EDGE_LOOP('',(#1074,#1075,#1076,#1077));
#312=EDGE_LOOP('',(#1078));
#313=EDGE_LOOP('',(#1079));
#314=EDGE_LOOP('',(#1080,#1081,#1082,#1083));
#315=EDGE_LOOP('',(#1084));
#316=EDGE_LOOP('',(#1085));
#317=EDGE_LOOP('',(#1086,#1087,#1088,#1089));
#318=EDGE_LOOP('',(#1090));
#319=EDGE_LOOP('',(#1091,#1092,#1093,#1094));
#320=EDGE_LOOP('',(#1095));
#321=EDGE_LOOP('',(#1096));
#322=EDGE_LOOP('',(#1097,#1098,#1099,#1100));
#323=EDGE_LOOP('',(#1101,#1102,#1103,#1104));
#324=EDGE_LOOP('',(#1105));
#325=EDGE_LOOP('',(#1106));
#326=EDGE_LOOP('',(#1107,#1108,#1109,#1110));
#327=EDGE_LOOP('',(#1111,#1112,#1113));
#431=LINE('',#2326,#541);
#432=LINE('',#2329,#542);
#433=LINE('',#2333,#543);
#434=LINE('',#2339,#544);
#435=LINE('',#2347,#545);
#436=LINE('',#2355,#546);
#437=LINE('',#2362,#547);
#438=LINE('',#2365,#548);
#439=LINE('',#2371,#549);
#541=VECTOR('',#1856,1.);
#542=VECTOR('',#1859,1.1);
#543=VECTOR('',#1864,2.);
#544=VECTOR('',#1873,1.9);
#545=VECTOR('',#1882,1.);
#546=VECTOR('',#1893,1.);
#547=VECTOR('',#1902,2.);
#548=VECTOR('',#1905,1.9);
#549=VECTOR('',#1914,1.1);
#640=CIRCLE('',#1608,2.);
#641=CIRCLE('',#1609,1.);
#642=CIRCLE('',#1611,1.);
#643=CIRCLE('',#1613,1.2);
#644=CIRCLE('',#1615,2.);
#645=CIRCLE('',#1617,1.8);
#646=CIRCLE('',#1620,1.);
#647=CIRCLE('',#1621,0.866025403784439);
#648=CIRCLE('',#1623,1.);
#649=CIRCLE('',#1625,1.);
#650=CIRCLE('',#1627,1.);
#651=CIRCLE('',#1629,2.);
#652=CIRCLE('',#1631,2.);
#653=CIRCLE('',#1633,1.8);
#654=CIRCLE('',#1635,1.2);
#655=CIRCLE('',#1638,1.);
#721=VERTEX_POINT('',#2319);
#722=VERTEX_POINT('',#2321);
#723=VERTEX_POINT('',#2324);
#724=VERTEX_POINT('',#2328);
#725=VERTEX_POINT('',#2332);
#726=VERTEX_POINT('',#2336);
#727=VERTEX_POINT('',#2341);
#728=VERTEX_POINT('',#2343);
#729=VERTEX_POINT('',#2346);
#730=VERTEX_POINT('',#2350);
#731=VERTEX_POINT('',#2353);
#732=VERTEX_POINT('',#2357);
#733=VERTEX_POINT('',#2360);
#734=VERTEX_POINT('',#2364);
#735=VERTEX_POINT('',#2368);
#736=VERTEX_POINT('',#2373);
#850=EDGE_CURVE('',#721,#721,#640,.T.);
#851=EDGE_CURVE('',#722,#722,#641,.T.);
#852=EDGE_CURVE('',#723,#723,#642,.T.);
#853=EDGE_CURVE('',#723,#722,#431,.T.);
#854=EDGE_CURVE('',#723,#724,#432,.T.);
#855=EDGE_CURVE('',#724,#724,#643,.T.);
#856=EDGE_CURVE('',#721,#725,#433,.T.);
#857=EDGE_CURVE('',#725,#725,#644,.T.);
#858=EDGE_CURVE('',#726,#726,#645,.T.);
#859=EDGE_CURVE('',#725,#726,#434,.T.);
#860=EDGE_CURVE('',#727,#727,#646,.T.);
#861=EDGE_CURVE('',#728,#728,#647,.T.);
#862=EDGE_CURVE('',#727,#729,#435,.T.);
#863=EDGE_CURVE('',#729,#729,#648,.T.);
#864=EDGE_CURVE('',#730,#730,#649,.T.);
#865=EDGE_CURVE('',#731,#731,#650,.T.);
#866=EDGE_CURVE('',#731,#730,#436,.T.);
#867=EDGE_CURVE('',#732,#732,#651,.T.);
#868=EDGE_CURVE('',#733,#733,#652,.T.);
#869=EDGE_CURVE('',#733,#732,#437,.T.);
#870=EDGE_CURVE('',#733,#734,#438,.T.);
#871=EDGE_CURVE('',#734,#734,#653,.T.);
#872=EDGE_CURVE('',#735,#735,#654,.T.);
#873=EDGE_CURVE('',#729,#735,#439,.T.);
#874=EDGE_CURVE('',#728,#736,#655,.T.);
#1064=ORIENTED_EDGE('',*,*,#850,.T.);
#1065=ORIENTED_EDGE('',*,*,#851,.T.);
#1066=ORIENTED_EDGE('',*,*,#852,.F.);
#1067=ORIENTED_EDGE('',*,*,#853,.T.);
#1068=ORIENTED_EDGE('',*,*,#851,.F.);
#1069=ORIENTED_EDGE('',*,*,#853,.F.);
#1070=ORIENTED_EDGE('',*,*,#852,.T.);
#1071=ORIENTED_EDGE('',*,*,#854,.T.);
#1072=ORIENTED_EDGE('',*,*,#855,.T.);
#1073=ORIENTED_EDGE('',*,*,#854,.F.);
#1074=ORIENTED_EDGE('',*,*,#850,.F.);
#1075=ORIENTED_EDGE('',*,*,#856,.T.);
#1076=ORIENTED_EDGE('',*,*,#857,.F.);
#1077=ORIENTED_EDGE('',*,*,#856,.F.);
#1078=ORIENTED_EDGE('',*,*,#858,.F.);
#1079=ORIENTED_EDGE('',*,*,#855,.F.);
#1080=ORIENTED_EDGE('',*,*,#857,.T.);
#1081=ORIENTED_EDGE('',*,*,#859,.T.);
#1082=ORIENTED_EDGE('',*,*,#858,.T.);
#1083=ORIENTED_EDGE('',*,*,#859,.F.);
#1084=ORIENTED_EDGE('',*,*,#860,.T.);
#1085=ORIENTED_EDGE('',*,*,#861,.T.);
#1086=ORIENTED_EDGE('',*,*,#860,.F.);
#1087=ORIENTED_EDGE('',*,*,#862,.T.);
#1088=ORIENTED_EDGE('',*,*,#863,.T.);
#1089=ORIENTED_EDGE('',*,*,#862,.F.);
#1090=ORIENTED_EDGE('',*,*,#864,.T.);
#1091=ORIENTED_EDGE('',*,*,#865,.T.);
#1092=ORIENTED_EDGE('',*,*,#866,.T.);
#1093=ORIENTED_EDGE('',*,*,#864,.F.);
#1094=ORIENTED_EDGE('',*,*,#866,.F.);
#1095=ORIENTED_EDGE('',*,*,#867,.F.);
#1096=ORIENTED_EDGE('',*,*,#865,.F.);
#1097=ORIENTED_EDGE('',*,*,#868,.F.);
#1098=ORIENTED_EDGE('',*,*,#869,.T.);
#1099=ORIENTED_EDGE('',*,*,#867,.T.);
#1100=ORIENTED_EDGE('',*,*,#869,.F.);
#1101=ORIENTED_EDGE('',*,*,#868,.T.);
#1102=ORIENTED_EDGE('',*,*,#870,.T.);
#1103=ORIENTED_EDGE('',*,*,#871,.T.);
#1104=ORIENTED_EDGE('',*,*,#870,.F.);
#1105=ORIENTED_EDGE('',*,*,#871,.F.);
#1106=ORIENTED_EDGE('',*,*,#872,.F.);
#1107=ORIENTED_EDGE('',*,*,#863,.F.);
#1108=ORIENTED_EDGE('',*,*,#873,.T.);
#1109=ORIENTED_EDGE('',*,*,#872,.T.);
#1110=ORIENTED_EDGE('',*,*,#873,.F.);
#1111=ORIENTED_EDGE('',*,*,#861,.F.);
#1112=ORIENTED_EDGE('',*,*,#874,.T.);
#1113=ORIENTED_EDGE('',*,*,#874,.F.);
#1363=CONICAL_SURFACE('',#1612,1.1,0.785398163397448);
#1364=CONICAL_SURFACE('',#1618,1.9,0.785398163397448);
#1365=CONICAL_SURFACE('',#1632,1.9,0.785398163397448);
#1366=CONICAL_SURFACE('',#1636,1.1,0.785398163397448);
#1395=ADVANCED_FACE('',(#204,#114),#145,.F.);
#1396=ADVANCED_FACE('',(#205),#91,.F.);
#1397=ADVANCED_FACE('',(#206),#1363,.F.);
#1398=ADVANCED_FACE('',(#207),#92,.T.);
#1399=ADVANCED_FACE('',(#208,#115),#146,.T.);
#1400=ADVANCED_FACE('',(#209),#1364,.T.);
#1401=ADVANCED_FACE('',(#210,#116),#147,.F.);
#1402=ADVANCED_FACE('',(#211),#93,.T.);
#1403=ADVANCED_FACE('',(#212),#148,.T.);
#1404=ADVANCED_FACE('',(#213),#94,.T.);
#1405=ADVANCED_FACE('',(#214,#117),#149,.T.);
#1406=ADVANCED_FACE('',(#215),#95,.T.);
#1407=ADVANCED_FACE('',(#216),#1365,.T.);
#1408=ADVANCED_FACE('',(#217,#118),#150,.F.);
#1409=ADVANCED_FACE('',(#218),#1366,.F.);
#1410=ADVANCED_FACE('',(#219),#43,.F.);
#1477=CLOSED_SHELL('',(#1395,#1396,#1397,#1398,#1399,#1400));
#1478=CLOSED_SHELL('',(#1401,#1402,#1403,#1404,#1405,#1406,#1407,#1408,
#1409,#1410));
#1606=AXIS2_PLACEMENT_3D('',#2317,#1844,#1845);
#1607=AXIS2_PLACEMENT_3D('',#2318,#1846,#1847);
#1608=AXIS2_PLACEMENT_3D('',#2320,#1848,#1849);
#1609=AXIS2_PLACEMENT_3D('',#2322,#1850,#1851);
#1610=AXIS2_PLACEMENT_3D('',#2323,#1852,#1853);
#1611=AXIS2_PLACEMENT_3D('',#2325,#1854,#1855);
#1612=AXIS2_PLACEMENT_3D('',#2327,#1857,#1858);
#1613=AXIS2_PLACEMENT_3D('',#2330,#1860,#1861);
#1614=AXIS2_PLACEMENT_3D('',#2331,#1862,#1863);
#1615=AXIS2_PLACEMENT_3D('',#2334,#1865,#1866);
#1616=AXIS2_PLACEMENT_3D('',#2335,#1867,#1868);
#1617=AXIS2_PLACEMENT_3D('',#2337,#1869,#1870);
#1618=AXIS2_PLACEMENT_3D('',#2338,#1871,#1872);
#1619=AXIS2_PLACEMENT_3D('',#2340,#1874,#1875);
#1620=AXIS2_PLACEMENT_3D('',#2342,#1876,#1877);
#1621=AXIS2_PLACEMENT_3D('',#2344,#1878,#1879);
#1622=AXIS2_PLACEMENT_3D('',#2345,#1880,#1881);
#1623=AXIS2_PLACEMENT_3D('',#2348,#1883,#1884);
#1624=AXIS2_PLACEMENT_3D('',#2349,#1885,#1886);
#1625=AXIS2_PLACEMENT_3D('',#2351,#1887,#1888);
#1626=AXIS2_PLACEMENT_3D('',#2352,#1889,#1890);
#1627=AXIS2_PLACEMENT_3D('',#2354,#1891,#1892);
#1628=AXIS2_PLACEMENT_3D('',#2356,#1894,#1895);
#1629=AXIS2_PLACEMENT_3D('',#2358,#1896,#1897);
#1630=AXIS2_PLACEMENT_3D('',#2359,#1898,#1899);
#1631=AXIS2_PLACEMENT_3D('',#2361,#1900,#1901);
#1632=AXIS2_PLACEMENT_3D('',#2363,#1903,#1904);
#1633=AXIS2_PLACEMENT_3D('',#2366,#1906,#1907);
#1634=AXIS2_PLACEMENT_3D('',#2367,#1908,#1909);
#1635=AXIS2_PLACEMENT_3D('',#2369,#1910,#1911);
#1636=AXIS2_PLACEMENT_3D('',#2370,#1912,#1913);
#1637=AXIS2_PLACEMENT_3D('',#2372,#1915,#1916);
#1638=AXIS2_PLACEMENT_3D('',#2374,#1917,#1918);
#1844=DIRECTION('axis',(0.,0.,1.));
#1845=DIRECTION('refdir',(1.,0.,0.));
#1846=DIRECTION('center_axis',(0.,0.,1.));
#1847=DIRECTION('ref_axis',(-1.,0.,0.));
#1848=DIRECTION('center_axis',(0.,0.,-1.));
#1849=DIRECTION('ref_axis',(-1.,0.,0.));
#1850=DIRECTION('center_axis',(0.,0.,1.));
#1851=DIRECTION('ref_axis',(-1.,0.,0.));
#1852=DIRECTION('center_axis',(0.,0.,-1.));
#1853=DIRECTION('ref_axis',(-1.,0.,0.));
#1854=DIRECTION('center_axis',(0.,0.,-1.));
#1855=DIRECTION('ref_axis',(-1.,0.,0.));
#1856=DIRECTION('',(0.,0.,-1.));
#1857=DIRECTION('center_axis',(0.,0.,1.));
#1858=DIRECTION('ref_axis',(-1.,0.,0.));
#1859=DIRECTION('',(0.707106781186547,8.65956056235493E-17,0.707106781186548));
#1860=DIRECTION('center_axis',(0.,0.,1.));
#1861=DIRECTION('ref_axis',(-1.,0.,0.));
#1862=DIRECTION('center_axis',(0.,0.,-1.));
#1863=DIRECTION('ref_axis',(-1.,0.,0.));
#1864=DIRECTION('',(0.,0.,1.));
#1865=DIRECTION('center_axis',(0.,0.,1.));
#1866=DIRECTION('ref_axis',(-1.,0.,0.));
#1867=DIRECTION('center_axis',(0.,0.,1.));
#1868=DIRECTION('ref_axis',(-1.,0.,0.));
#1869=DIRECTION('center_axis',(0.,0.,-1.));
#1870=DIRECTION('ref_axis',(-1.,0.,0.));
#1871=DIRECTION('center_axis',(0.,0.,-1.));
#1872=DIRECTION('ref_axis',(-1.,0.,0.));
#1873=DIRECTION('',(-0.707106781186547,8.65956056235493E-17,0.707106781186548));
#1874=DIRECTION('center_axis',(0.,0.,1.));
#1875=DIRECTION('ref_axis',(-1.,0.,0.));
#1876=DIRECTION('center_axis',(0.,0.,-1.));
#1877=DIRECTION('ref_axis',(-1.,0.,0.));
#1878=DIRECTION('center_axis',(0.,0.,1.));
#1879=DIRECTION('ref_axis',(0.,-1.,0.));
#1880=DIRECTION('center_axis',(0.,0.,-1.));
#1881=DIRECTION('ref_axis',(-1.,0.,0.));
#1882=DIRECTION('',(0.,0.,1.));
#1883=DIRECTION('center_axis',(0.,0.,-1.));
#1884=DIRECTION('ref_axis',(-1.,0.,0.));
#1885=DIRECTION('center_axis',(0.,0.,1.));
#1886=DIRECTION('ref_axis',(-1.,0.,0.));
#1887=DIRECTION('center_axis',(0.,0.,1.));
#1888=DIRECTION('ref_axis',(-1.,0.,0.));
#1889=DIRECTION('center_axis',(0.,0.,-1.));
#1890=DIRECTION('ref_axis',(-1.,0.,0.));
#1891=DIRECTION('center_axis',(0.,0.,1.));
#1892=DIRECTION('ref_axis',(-1.,0.,0.));
#1893=DIRECTION('',(0.,0.,1.));
#1894=DIRECTION('center_axis',(0.,0.,1.));
#1895=DIRECTION('ref_axis',(-1.,0.,0.));
#1896=DIRECTION('center_axis',(0.,0.,-1.));
#1897=DIRECTION('ref_axis',(-1.,0.,0.));
#1898=DIRECTION('center_axis',(0.,0.,-1.));
#1899=DIRECTION('ref_axis',(-1.,0.,0.));
#1900=DIRECTION('center_axis',(0.,0.,-1.));
#1901=DIRECTION('ref_axis',(-1.,0.,0.));
#1902=DIRECTION('',(0.,0.,1.));
#1903=DIRECTION('center_axis',(0.,0.,1.));
#1904=DIRECTION('ref_axis',(-1.,0.,0.));
#1905=DIRECTION('',(-0.707106781186547,-8.65956056235493E-17,-0.707106781186548));
#1906=DIRECTION('center_axis',(0.,0.,1.));
#1907=DIRECTION('ref_axis',(-1.,0.,0.));
#1908=DIRECTION('center_axis',(0.,0.,1.));
#1909=DIRECTION('ref_axis',(-1.,0.,0.));
#1910=DIRECTION('center_axis',(0.,0.,-1.));
#1911=DIRECTION('ref_axis',(-1.,0.,0.));
#1912=DIRECTION('center_axis',(0.,0.,-1.));
#1913=DIRECTION('ref_axis',(-1.,0.,0.));
#1914=DIRECTION('',(0.707106781186547,-8.65956056235493E-17,-0.707106781186548));
#1915=DIRECTION('center_axis',(0.,0.,1.));
#1916=DIRECTION('ref_axis',(1.,0.,0.));
#1917=DIRECTION('center_axis',(0.,1.,0.));
#1918=DIRECTION('ref_axis',(-1.,0.,0.));
#2317=CARTESIAN_POINT('',(0.,0.,0.));
#2318=CARTESIAN_POINT('Origin',(8.,-7.5,10.5));
#2319=CARTESIAN_POINT('',(10.,-7.5,10.5));
#2320=CARTESIAN_POINT('Origin',(8.,-7.5,10.5));
#2321=CARTESIAN_POINT('',(9.,-7.5,10.5));
#2322=CARTESIAN_POINT('Origin',(8.,-7.5,10.5));
#2323=CARTESIAN_POINT('Origin',(8.,-7.5,12.5));
#2324=CARTESIAN_POINT('',(9.,-7.5,12.3));
#2325=CARTESIAN_POINT('Origin',(8.,-7.5,12.3));
#2326=CARTESIAN_POINT('',(9.,-7.5,12.5));
#2327=CARTESIAN_POINT('Origin',(8.,-7.5,12.4));
#2328=CARTESIAN_POINT('',(9.2,-7.5,12.5));
#2329=CARTESIAN_POINT('',(9.1,-7.5,12.4));
#2330=CARTESIAN_POINT('Origin',(8.,-7.5,12.5));
#2331=CARTESIAN_POINT('Origin',(8.,-7.5,12.5));
#2332=CARTESIAN_POINT('',(10.,-7.5,12.3));
#2333=CARTESIAN_POINT('',(10.,-7.5,12.5));
#2334=CARTESIAN_POINT('Origin',(8.,-7.5,12.3));
#2335=CARTESIAN_POINT('Origin',(8.,-7.5,12.5));
#2336=CARTESIAN_POINT('',(9.8,-7.5,12.5));
#2337=CARTESIAN_POINT('Origin',(8.,-7.5,12.5));
#2338=CARTESIAN_POINT('Origin',(8.,-7.5,12.4));
#2339=CARTESIAN_POINT('',(9.9,-7.5,12.4));
#2340=CARTESIAN_POINT('Origin',(8.,-7.5,4.5));
#2341=CARTESIAN_POINT('',(9.,-7.5,4.5));
#2342=CARTESIAN_POINT('Origin',(8.,-7.5,4.5));
#2343=CARTESIAN_POINT('',(7.13397459621556,-7.5,4.5));
#2344=CARTESIAN_POINT('Origin',(8.,-7.5,4.5));
#2345=CARTESIAN_POINT('Origin',(8.,-7.5,12.5));
#2346=CARTESIAN_POINT('',(9.,-7.5,6.7));
#2347=CARTESIAN_POINT('',(9.,-7.5,12.5));
#2348=CARTESIAN_POINT('Origin',(8.,-7.5,6.7));
#2349=CARTESIAN_POINT('Origin',(8.,-7.5,10.5));
#2350=CARTESIAN_POINT('',(9.,-7.5,10.5));
#2351=CARTESIAN_POINT('Origin',(8.,-7.5,10.5));
#2352=CARTESIAN_POINT('Origin',(8.,-7.5,12.5));
#2353=CARTESIAN_POINT('',(9.,-7.5,7.5));
#2354=CARTESIAN_POINT('Origin',(8.,-7.5,7.5));
#2355=CARTESIAN_POINT('',(9.,-7.5,12.5));
#2356=CARTESIAN_POINT('Origin',(8.,-7.5,7.5));
#2357=CARTESIAN_POINT('',(10.,-7.5,7.5));
#2358=CARTESIAN_POINT('Origin',(8.,-7.5,7.5));
#2359=CARTESIAN_POINT('Origin',(8.,-7.5,12.5));
#2360=CARTESIAN_POINT('',(10.,-7.5,6.7));
#2361=CARTESIAN_POINT('Origin',(8.,-7.5,6.7));
#2362=CARTESIAN_POINT('',(10.,-7.5,12.5));
#2363=CARTESIAN_POINT('Origin',(8.,-7.5,6.6));
#2364=CARTESIAN_POINT('',(9.8,-7.5,6.5));
#2365=CARTESIAN_POINT('',(9.9,-7.5,6.6));
#2366=CARTESIAN_POINT('Origin',(8.,-7.5,6.5));
#2367=CARTESIAN_POINT('Origin',(8.,-7.5,6.5));
#2368=CARTESIAN_POINT('',(9.2,-7.5,6.5));
#2369=CARTESIAN_POINT('Origin',(8.,-7.5,6.5));
#2370=CARTESIAN_POINT('Origin',(8.,-7.5,6.6));
#2371=CARTESIAN_POINT('',(9.1,-7.5,6.6));
#2372=CARTESIAN_POINT('Origin',(8.,-7.5,4.));
#2373=CARTESIAN_POINT('',(8.,-7.5,5.));
#2374=CARTESIAN_POINT('Origin',(8.,-7.5,4.));
#2659=UNCERTAINTY_MEASURE_WITH_UNIT(LENGTH_MEASURE(0.01),#2677,
'DISTANCE_ACCURACY_VALUE',
'Maximum model space distance between geometric entities at asserted c
onnectivities');
#2666=UNCERTAINTY_MEASURE_WITH_UNIT(LENGTH_MEASURE(0.01),#2677,
'DISTANCE_ACCURACY_VALUE',
'Maximum model space distance between geometric entities at asserted c
onnectivities');
#2669=(
GEOMETRIC_REPRESENTATION_CONTEXT(3)
GLOBAL_UNCERTAINTY_ASSIGNED_CONTEXT((#2659))
GLOBAL_UNIT_ASSIGNED_CONTEXT((#2677,#2679,#2680))
REPRESENTATION_CONTEXT('','3D')
);
#2676=(
GEOMETRIC_REPRESENTATION_CONTEXT(3)
GLOBAL_UNCERTAINTY_ASSIGNED_CONTEXT((#2666))
GLOBAL_UNIT_ASSIGNED_CONTEXT((#2677,#2679,#2680))
REPRESENTATION_CONTEXT('','3D')
);
#2677=(
LENGTH_UNIT()
NAMED_UNIT(*)
SI_UNIT(.MILLI.,.METRE.)
);
#2679=(
NAMED_UNIT(*)
PLANE_ANGLE_UNIT()
SI_UNIT($,.RADIAN.)
);
#2680=(
NAMED_UNIT(*)
SI_UNIT($,.STERADIAN.)
SOLID_ANGLE_UNIT()
);
#2683=SHAPE_DEFINITION_REPRESENTATION(#2692,#2709);
#2692=PRODUCT_DEFINITION_SHAPE('',$,#2719);
#2709=SHAPE_REPRESENTATION('',(#1606),#2669);
#2716=PRODUCT_DEFINITION_CONTEXT('part definition',#2745,'design');
#2719=PRODUCT_DEFINITION('Screw_02','Screw_02',#2728,#2716);
#2728=PRODUCT_DEFINITION_FORMATION('',$,#2749);
#2745=APPLICATION_CONTEXT(
'Core Data for Automotive Mechanical Design Process');
#2746=PRODUCT_CONTEXT('part definition',#2745,'mechanical');
#2749=PRODUCT('Screw_02','Screw_02',$,(#2746));
#2757=PRESENTATION_STYLE_ASSIGNMENT((#2759));
#2759=SURFACE_STYLE_USAGE(.BOTH.,#2761);
#2761=SURFACE_SIDE_STYLE('',(#2763));
#2763=SURFACE_STYLE_FILL_AREA(#2765);
#2765=FILL_AREA_STYLE('Opaque(203,203,203)',(#2767));
#2767=FILL_AREA_STYLE_COLOUR('Opaque(203,203,203)',#2769);
#2769=COLOUR_RGB('Opaque(203,203,203)', 0.09019608, 0.27058824, 0.51372549);
ENDSEC;
END-ISO-10303-21;
